ISO-10303-21;
HEADER;
/* Generated by software containing ST-Developer
 * from STEP Tools, Inc. (www.steptools.com) 
 */

FILE_DESCRIPTION(
/* description */ ('Fatigue rig crank-slider'),
/* implementation_level */ '2;1');

FILE_NAME(
/* name */ 'Bearing bolt reducer (2).step',
/* time_stamp */ '2026-10-28T03:24:50-07:00',
/* author */ (''),
/* organization */ (''),
/* preprocessor_version */ 'ST-DEVELOPER v20.2',
/* originating_system */ 'Autodesk Translation Framework v15.17.0.0',
/* authorisation */ '');

FILE_SCHEMA (('AUTOMOTIVE_DESIGN { 1 0 10303 214 3 1 1 }'));
ENDSEC;

DATA;
#10=MECHANICAL_DESIGN_GEOMETRIC_PRESENTATION_REPRESENTATION('',(#592),#16911);
#492=SHAPE_REPRESENTATION_RELATIONSHIP('SRR','None',#17131,#542);
#542=ADVANCED_BREP_SHAPE_REPRESENTATION('',(#651),#16860);
#592=STYLED_ITEM('',(#17494),#651);
#651=MANIFOLD_SOLID_BREP('Body1',#8883);
#756=FACE_BOUND('',#1869,.T.);
#757=FACE_BOUND('',#1871,.T.);
#931=PLANE('',#9649);
#932=PLANE('',#9650);
#1287=FACE_OUTER_BOUND('',#1866,.T.);
#1288=FACE_OUTER_BOUND('',#1867,.T.);
#1289=FACE_OUTER_BOUND('',#1868,.T.);
#1290=FACE_OUTER_BOUND('',#1870,.T.);
#1866=EDGE_LOOP('',(#6284,#6285,#6286,#6287));
#1867=EDGE_LOOP('',(#6288,#6289,#6290,#6291));
#1868=EDGE_LOOP('',(#6292));
#1869=EDGE_LOOP('',(#6293));
#1870=EDGE_LOOP('',(#6294));
#1871=EDGE_LOOP('',(#6295));
#2532=LINE('',#13680,#3178);
#2533=LINE('',#13686,#3179);
#3178=VECTOR('',#10942,0.425);
#3179=VECTOR('',#10949,0.645);
#3824=CIRCLE('',#9644,0.425);
#3825=CIRCLE('',#9645,0.425);
#3826=CIRCLE('',#9647,0.645);
#3827=CIRCLE('',#9648,0.645);
#4248=VERTEX_POINT('',#13677);
#4249=VERTEX_POINT('',#13679);
#4250=VERTEX_POINT('',#13683);
#4251=VERTEX_POINT('',#13685);
#5040=EDGE_CURVE('',#4248,#4248,#3824,.T.);
#5041=EDGE_CURVE('',#4248,#4249,#2532,.T.);
#5042=EDGE_CURVE('',#4249,#4249,#3825,.T.);
#5043=EDGE_CURVE('',#4250,#4250,#3826,.T.);
#5044=EDGE_CURVE('',#4250,#4251,#2533,.T.);
#5045=EDGE_CURVE('',#4251,#4251,#3827,.T.);
#6284=ORIENTED_EDGE('',*,*,#5040,.F.);
#6285=ORIENTED_EDGE('',*,*,#5041,.T.);
#6286=ORIENTED_EDGE('',*,*,#5042,.T.);
#6287=ORIENTED_EDGE('',*,*,#5041,.F.);
#6288=ORIENTED_EDGE('',*,*,#5043,.F.);
#6289=ORIENTED_EDGE('',*,*,#5044,.T.);
#6290=ORIENTED_EDGE('',*,*,#5045,.T.);
#6291=ORIENTED_EDGE('',*,*,#5044,.F.);
#6292=ORIENTED_EDGE('',*,*,#5043,.T.);
#6293=ORIENTED_EDGE('',*,*,#5040,.T.);
#6294=ORIENTED_EDGE('',*,*,#5045,.F.);
#6295=ORIENTED_EDGE('',*,*,#5042,.F.);
#8232=CYLINDRICAL_SURFACE('',#9643,0.425);
#8233=CYLINDRICAL_SURFACE('',#9646,0.645);
#8425=ADVANCED_FACE('',(#1287),#8232,.F.);
#8426=ADVANCED_FACE('',(#1288),#8233,.T.);
#8427=ADVANCED_FACE('',(#1289,#756),#931,.T.);
#8428=ADVANCED_FACE('',(#1290,#757),#932,.F.);
#8883=CLOSED_SHELL('',(#8425,#8426,#8427,#8428));
#9642=AXIS2_PLACEMENT_3D('',#13675,#10936,#10937);
#9643=AXIS2_PLACEMENT_3D('',#13676,#10938,#10939);
#9644=AXIS2_PLACEMENT_3D('',#13678,#10940,#10941);
#9645=AXIS2_PLACEMENT_3D('',#13681,#10943,#10944);
#9646=AXIS2_PLACEMENT_3D('',#13682,#10945,#10946);
#9647=AXIS2_PLACEMENT_3D('',#13684,#10947,#10948);
#9648=AXIS2_PLACEMENT_3D('',#13687,#10950,#10951);
#9649=AXIS2_PLACEMENT_3D('',#13688,#10952,#10953);
#9650=AXIS2_PLACEMENT_3D('',#13689,#10954,#10955);
#10936=DIRECTION('axis',(0.,0.,1.));
#10937=DIRECTION('refdir',(1.,0.,0.));
#10938=DIRECTION('center_axis',(0.,0.,1.));
#10939=DIRECTION('ref_axis',(1.,0.,0.));
#10940=DIRECTION('center_axis',(0.,0.,-1.));
#10941=DIRECTION('ref_axis',(1.,0.,0.));
#10942=DIRECTION('',(0.,0.,-1.));
#10943=DIRECTION('center_axis',(0.,0.,-1.));
#10944=DIRECTION('ref_axis',(1.,0.,0.));
#10945=DIRECTION('center_axis',(0.,0.,1.));
#10946=DIRECTION('ref_axis',(1.,0.,0.));
#10947=DIRECTION('center_axis',(0.,0.,1.));
#10948=DIRECTION('ref_axis',(1.,0.,0.));
#10949=DIRECTION('',(0.,0.,-1.));
#10950=DIRECTION('center_axis',(0.,0.,1.));
#10951=DIRECTION('ref_axis',(1.,0.,0.));
#10952=DIRECTION('center_axis',(0.,0.,1.));
#10953=DIRECTION('ref_axis',(1.,0.,0.));
#10954=DIRECTION('center_axis',(0.,0.,1.));
#10955=DIRECTION('ref_axis',(1.,0.,0.));
#13675=CARTESIAN_POINT('',(0.,0.,0.));
#13676=CARTESIAN_POINT('Origin',(-4.75,-7.,8.67));
#13677=CARTESIAN_POINT('',(-5.175,-7.,9.87));
#13678=CARTESIAN_POINT('Origin',(-4.75,-7.,9.87));
#13679=CARTESIAN_POINT('',(-5.175,-7.,8.67));
#13680=CARTESIAN_POINT('',(-5.175,-7.,8.67));
#13681=CARTESIAN_POINT('Origin',(-4.75,-7.,8.67));
#13682=CARTESIAN_POINT('Origin',(-4.75,-7.,8.67));
#13683=CARTESIAN_POINT('',(-5.395,-7.,9.87));
#13684=CARTESIAN_POINT('Origin',(-4.75,-7.,9.87));
#13685=CARTESIAN_POINT('',(-5.395,-7.,8.67));
#13686=CARTESIAN_POINT('',(-5.395,-7.,8.67));
#13687=CARTESIAN_POINT('Origin',(-4.75,-7.,8.67));
#13688=CARTESIAN_POINT('Origin',(-4.75,-7.,9.87));
#13689=CARTESIAN_POINT('Origin',(-4.75,-7.,8.67));
#16801=UNCERTAINTY_MEASURE_WITH_UNIT(LENGTH_MEASURE(0.001),#16912,
'DISTANCE_ACCURACY_VALUE',
'Maximum model space distance between geometric entities at asserted c
onnectivities');
#16852=UNCERTAINTY_MEASURE_WITH_UNIT(LENGTH_MEASURE(0.001),#16912,
'DISTANCE_ACCURACY_VALUE',
'Maximum model space distance between geometric entities at asserted c
onnectivities');
#16860=(
GEOMETRIC_REPRESENTATION_CONTEXT(3)
GLOBAL_UNCERTAINTY_ASSIGNED_CONTEXT((#16801))
GLOBAL_UNIT_ASSIGNED_CONTEXT((#16912,#16914,#16915))
REPRESENTATION_CONTEXT('','3D')
);
#16911=(
GEOMETRIC_REPRESENTATION_CONTEXT(3)
GLOBAL_UNCERTAINTY_ASSIGNED_CONTEXT((#16852))
GLOBAL_UNIT_ASSIGNED_CONTEXT((#16912,#16914,#16915))
REPRESENTATION_CONTEXT('','3D')
);
#16912=(
LENGTH_UNIT()
NAMED_UNIT(*)
SI_UNIT(.CENTI.,.METRE.)
);
#16914=(
NAMED_UNIT(*)
PLANE_ANGLE_UNIT()
SI_UNIT($,.RADIAN.)
);
#16915=(
NAMED_UNIT(*)
SI_UNIT($,.STERADIAN.)
SOLID_ANGLE_UNIT()
);
#16923=SHAPE_DEFINITION_REPRESENTATION(#16981,#17131);
#16981=PRODUCT_DEFINITION_SHAPE('',$,#17190);
#17131=SHAPE_REPRESENTATION('',(#9642),#16860);
#17182=PRODUCT_DEFINITION_CONTEXT('part definition',#17358,'design');
#17190=PRODUCT_DEFINITION('Bearing bolt reducer (2)',
'Bearing bolt reducer (2)',#17248,#17182);
#17248=PRODUCT_DEFINITION_FORMATION('',$,#17367);
#17358=APPLICATION_CONTEXT(
'Core Data for Automotive Mechanical Design Process');
#17359=PRODUCT_CONTEXT('part definition',#17358,'mechanical');
#17367=PRODUCT('Bearing bolt reducer (2)','Bearing bolt reducer (2)',
'Bearing bolt reducer (2)',(#17359));
#17488=COLOUR_RGB('Black',0.12,0.14,0.17);
#17489=FILL_AREA_STYLE_COLOUR('',#17488);
#17490=FILL_AREA_STYLE('',(#17489));
#17491=SURFACE_STYLE_FILL_AREA(#17490);
#17492=SURFACE_SIDE_STYLE('',(#17491));
#17493=SURFACE_STYLE_USAGE(.BOTH.,#17492);
#17494=PRESENTATION_STYLE_ASSIGNMENT((#17493));
ENDSEC;
END-ISO-10303-21;
